ISO-10303-21;
HEADER;
/* Generated by software containing ST-Developer
 * from STEP Tools, Inc. (www.steptools.com) 
 */

FILE_DESCRIPTION(
/* description */ ('Hand-crank flanged shaft unit'),
/* implementation_level */ '2;1');

FILE_NAME(
/* name */ 'Flange bolt sleeve (6).step',
/* time_stamp */ '2026-10-27T18:35:45-07:00',
/* author */ (''),
/* organization */ (''),
/* preprocessor_version */ 'ST-DEVELOPER v20.2',
/* originating_system */ 'Autodesk Translation Framework v15.17.0.0',
/* authorisation */ '');

FILE_SCHEMA (('AUTOMOTIVE_DESIGN { 1 0 10303 214 3 1 1 }'));
ENDSEC;

DATA;
#10=MECHANICAL_DESIGN_GEOMETRIC_PRESENTATION_REPRESENTATION('',(#286),#6805);
#246=SHAPE_REPRESENTATION_RELATIONSHIP('SRR','None',#6907,#266);
#266=ADVANCED_BREP_SHAPE_REPRESENTATION('',(#307),#6790);
#286=STYLED_ITEM('',(#7098),#307);
#307=MANIFOLD_SOLID_BREP('Body1',#3327);
#354=FACE_BOUND('',#790,.T.);
#355=FACE_BOUND('',#792,.T.);
#438=PLANE('',#3662);
#439=PLANE('',#3663);
#565=FACE_OUTER_BOUND('',#787,.T.);
#566=FACE_OUTER_BOUND('',#788,.T.);
#567=FACE_OUTER_BOUND('',#789,.T.);
#568=FACE_OUTER_BOUND('',#791,.T.);
#787=EDGE_LOOP('',(#2455,#2456,#2457,#2458));
#788=EDGE_LOOP('',(#2459,#2460,#2461,#2462));
#789=EDGE_LOOP('',(#2463));
#790=EDGE_LOOP('',(#2464));
#791=EDGE_LOOP('',(#2465));
#792=EDGE_LOOP('',(#2466));
#1039=LINE('',#5166,#1267);
#1040=LINE('',#5172,#1268);
#1267=VECTOR('',#4206,0.425);
#1268=VECTOR('',#4213,0.595);
#1481=CIRCLE('',#3657,0.425);
#1482=CIRCLE('',#3658,0.425);
#1483=CIRCLE('',#3660,0.595);
#1484=CIRCLE('',#3661,0.595);
#1637=VERTEX_POINT('',#5163);
#1638=VERTEX_POINT('',#5165);
#1639=VERTEX_POINT('',#5169);
#1640=VERTEX_POINT('',#5171);
#1945=EDGE_CURVE('',#1637,#1637,#1481,.T.);
#1946=EDGE_CURVE('',#1637,#1638,#1039,.T.);
#1947=EDGE_CURVE('',#1638,#1638,#1482,.T.);
#1948=EDGE_CURVE('',#1639,#1639,#1483,.T.);
#1949=EDGE_CURVE('',#1639,#1640,#1040,.T.);
#1950=EDGE_CURVE('',#1640,#1640,#1484,.T.);
#2455=ORIENTED_EDGE('',*,*,#1945,.F.);
#2456=ORIENTED_EDGE('',*,*,#1946,.T.);
#2457=ORIENTED_EDGE('',*,*,#1947,.T.);
#2458=ORIENTED_EDGE('',*,*,#1946,.F.);
#2459=ORIENTED_EDGE('',*,*,#1948,.F.);
#2460=ORIENTED_EDGE('',*,*,#1949,.T.);
#2461=ORIENTED_EDGE('',*,*,#1950,.T.);
#2462=ORIENTED_EDGE('',*,*,#1949,.F.);
#2463=ORIENTED_EDGE('',*,*,#1948,.T.);
#2464=ORIENTED_EDGE('',*,*,#1945,.T.);
#2465=ORIENTED_EDGE('',*,*,#1950,.F.);
#2466=ORIENTED_EDGE('',*,*,#1947,.F.);
#3089=CYLINDRICAL_SURFACE('',#3656,0.425);
#3090=CYLINDRICAL_SURFACE('',#3659,0.595);
#3182=ADVANCED_FACE('',(#565),#3089,.F.);
#3183=ADVANCED_FACE('',(#566),#3090,.T.);
#3184=ADVANCED_FACE('',(#567,#354),#438,.T.);
#3185=ADVANCED_FACE('',(#568,#355),#439,.F.);
#3327=CLOSED_SHELL('',(#3182,#3183,#3184,#3185));
#3655=AXIS2_PLACEMENT_3D('',#5161,#4200,#4201);
#3656=AXIS2_PLACEMENT_3D('',#5162,#4202,#4203);
#3657=AXIS2_PLACEMENT_3D('',#5164,#4204,#4205);
#3658=AXIS2_PLACEMENT_3D('',#5167,#4207,#4208);
#3659=AXIS2_PLACEMENT_3D('',#5168,#4209,#4210);
#3660=AXIS2_PLACEMENT_3D('',#5170,#4211,#4212);
#3661=AXIS2_PLACEMENT_3D('',#5173,#4214,#4215);
#3662=AXIS2_PLACEMENT_3D('',#5174,#4216,#4217);
#3663=AXIS2_PLACEMENT_3D('',#5175,#4218,#4219);
#4200=DIRECTION('axis',(0.,0.,1.));
#4201=DIRECTION('refdir',(1.,0.,0.));
#4202=DIRECTION('center_axis',(0.,1.,0.));
#4203=DIRECTION('ref_axis',(1.,0.,0.));
#4204=DIRECTION('center_axis',(0.,-1.,0.));
#4205=DIRECTION('ref_axis',(1.,0.,0.));
#4206=DIRECTION('',(0.,-1.,0.));
#4207=DIRECTION('center_axis',(0.,-1.,0.));
#4208=DIRECTION('ref_axis',(1.,0.,0.));
#4209=DIRECTION('center_axis',(0.,1.,0.));
#4210=DIRECTION('ref_axis',(1.,0.,0.));
#4211=DIRECTION('center_axis',(0.,1.,0.));
#4212=DIRECTION('ref_axis',(1.,0.,0.));
#4213=DIRECTION('',(0.,-1.,0.));
#4214=DIRECTION('center_axis',(0.,1.,0.));
#4215=DIRECTION('ref_axis',(1.,0.,0.));
#4216=DIRECTION('center_axis',(0.,1.,0.));
#4217=DIRECTION('ref_axis',(1.,0.,0.));
#4218=DIRECTION('center_axis',(0.,1.,0.));
#4219=DIRECTION('ref_axis',(1.,0.,0.));
#5161=CARTESIAN_POINT('',(0.,0.,0.));
#5162=CARTESIAN_POINT('Origin',(3.2,21.,4.3));
#5163=CARTESIAN_POINT('',(2.775,22.,4.3));
#5164=CARTESIAN_POINT('Origin',(3.2,22.,4.3));
#5165=CARTESIAN_POINT('',(2.775,21.,4.3));
#5166=CARTESIAN_POINT('',(2.775,21.,4.3));
#5167=CARTESIAN_POINT('Origin',(3.2,21.,4.3));
#5168=CARTESIAN_POINT('Origin',(3.2,21.,4.3));
#5169=CARTESIAN_POINT('',(2.605,22.,4.3));
#5170=CARTESIAN_POINT('Origin',(3.2,22.,4.3));
#5171=CARTESIAN_POINT('',(2.605,21.,4.3));
#5172=CARTESIAN_POINT('',(2.605,21.,4.3));
#5173=CARTESIAN_POINT('Origin',(3.2,21.,4.3));
#5174=CARTESIAN_POINT('Origin',(3.2,22.,4.3));
#5175=CARTESIAN_POINT('Origin',(3.2,21.,4.3));
#6765=UNCERTAINTY_MEASURE_WITH_UNIT(LENGTH_MEASURE(0.001),#6806,
'DISTANCE_ACCURACY_VALUE',
'Maximum model space distance between geometric entities at asserted c
onnectivities');
#6780=UNCERTAINTY_MEASURE_WITH_UNIT(LENGTH_MEASURE(0.001),#6806,
'DISTANCE_ACCURACY_VALUE',
'Maximum model space distance between geometric entities at asserted c
onnectivities');
#6790=(
GEOMETRIC_REPRESENTATION_CONTEXT(3)
GLOBAL_UNCERTAINTY_ASSIGNED_CONTEXT((#6765))
GLOBAL_UNIT_ASSIGNED_CONTEXT((#6806,#6808,#6809))
REPRESENTATION_CONTEXT('','3D')
);
#6805=(
GEOMETRIC_REPRESENTATION_CONTEXT(3)
GLOBAL_UNCERTAINTY_ASSIGNED_CONTEXT((#6780))
GLOBAL_UNIT_ASSIGNED_CONTEXT((#6806,#6808,#6809))
REPRESENTATION_CONTEXT('','3D')
);
#6806=(
LENGTH_UNIT()
NAMED_UNIT(*)
SI_UNIT(.CENTI.,.METRE.)
);
#6808=(
NAMED_UNIT(*)
PLANE_ANGLE_UNIT()
SI_UNIT($,.RADIAN.)
);
#6809=(
NAMED_UNIT(*)
SI_UNIT($,.STERADIAN.)
SOLID_ANGLE_UNIT()
);
#6819=SHAPE_DEFINITION_REPRESENTATION(#6843,#6907);
#6843=PRODUCT_DEFINITION_SHAPE('',$,#6932);
#6907=SHAPE_REPRESENTATION('',(#3655),#6790);
#6922=PRODUCT_DEFINITION_CONTEXT('part definition',#6996,'design');
#6932=PRODUCT_DEFINITION('Flange bolt sleeve (6)',
'Flange bolt sleeve (6)',#6956,#6922);
#6956=PRODUCT_DEFINITION_FORMATION('',$,#7007);
#6996=APPLICATION_CONTEXT(
'Core Data for Automotive Mechanical Design Process');
#6997=PRODUCT_CONTEXT('part definition',#6996,'mechanical');
#7007=PRODUCT('Flange bolt sleeve (6)','Flange bolt sleeve (6)',
'Flange bolt sleeve (6)',(#6997));
#7092=COLOUR_RGB('Black',0.12,0.14,0.17);
#7093=FILL_AREA_STYLE_COLOUR('',#7092);
#7094=FILL_AREA_STYLE('',(#7093));
#7095=SURFACE_STYLE_FILL_AREA(#7094);
#7096=SURFACE_SIDE_STYLE('',(#7095));
#7097=SURFACE_STYLE_USAGE(.BOTH.,#7096);
#7098=PRESENTATION_STYLE_ASSIGNMENT((#7097));
ENDSEC;
END-ISO-10303-21;
